ISO-10303-21;
HEADER;
FILE_DESCRIPTION (('STEP AP203'),
    '1' );
FILE_NAME ('1602p_c_44.step',
    '2026-10-31T14:11:27',
    ( '' ),
    ( '' ),
    'SwSTEP 2.0',
    'SolidWorks 2024',
    '' );
FILE_SCHEMA (( 'AUTOMOTIVE_DESIGN' ));
ENDSEC;

DATA;
#22=EDGE_LOOP ( 'NONE', ( #6663, #15564, #14189, #16631, #9667 ) ) ;
#90=VERTEX_POINT ( 'NONE', #12158 ) ;
#108=EDGE_CURVE ( 'NONE', #467, #12098, #6515, .T. ) ;
#110=AXIS2_PLACEMENT_3D ( 'NONE', #13114, #22230, #618 ) ;
#113=ORIENTED_EDGE ( 'NONE', *, *, #18987, .F. ) ;
#203=CARTESIAN_POINT ( 'NONE',  ( 34.89491389100820129, 23.30074776265919922, 13.00000000000000000 ) ) ;
#247=CARTESIAN_POINT ( 'NONE',  ( 34.40839383886530101, 23.41606575285529956, 13.00000000000000000 ) ) ;
#265=DIRECTION ( 'NONE',  ( 0.000000000000000000, -1.000000000000000000, 9.355573283744330345E-16 ) ) ;
#291=CARTESIAN_POINT ( 'NONE',  ( 36.76586756491558816, 21.07724224331888863, 12.00000000000000000 ) ) ;
#324=ADVANCED_FACE ( 'NONE', ( #917 ), #12711, .F. ) ;
#340=ADVANCED_FACE ( 'NONE', ( #13754 ), #20997, .F. ) ;
#346=CARTESIAN_POINT ( 'NONE',  ( 38.13838090529419844, 22.53196116135185179, 13.00000000000000000 ) ) ;
#354=AXIS2_PLACEMENT_3D ( 'NONE', #13719, #17407, #13844 ) ;
#373=ORIENTED_EDGE ( 'NONE', *, *, #19520, .F. ) ;
#392=DIRECTION ( 'NONE',  ( -0.1997366180463769070, -0.8426774492125652660, 0.5000000000000002220 ) ) ;
#415=DIRECTION ( 'NONE',  ( 1.000000000000000000, 0.000000000000000000, 0.000000000000000000 ) ) ;
#459=ORIENTED_EDGE ( 'NONE', *, *, #16927, .F. ) ;
#467=VERTEX_POINT ( 'NONE', #8539 ) ;
#476=EDGE_CURVE ( 'NONE', #6299, #3647, #15768, .T. ) ;
#486=MECHANICAL_CONTEXT ( 'NONE', #13521, 'mechanical' ) ;
#531=EDGE_LOOP ( 'NONE', ( #9595, #23275, #15737, #7809 ) ) ;
#534=DIRECTION ( 'NONE',  ( 0.9730401042858036753, -0.2306359803922031493, -5.432877459303553216E-17 ) ) ;
#556=AXIS2_PLACEMENT_3D ( 'NONE', #1022, #22638, #22995 ) ;
#618=DIRECTION ( 'NONE',  ( 0.000000000000000000, 0.000000000000000000, 1.000000000000000000 ) ) ;
#633=CARTESIAN_POINT ( 'NONE',  ( 34.40839383886530101, 23.41606575285529956, 13.00000000000000000 ) ) ;
#657=EDGE_CURVE ( 'NONE', #23364, #20134, #2455, .T. ) ;
#677=VERTEX_POINT ( 'NONE', #6121 ) ;
#743=( GEOMETRIC_REPRESENTATION_CONTEXT ( 3 ) GLOBAL_UNCERTAINTY_ASSIGNED_CONTEXT ( ( #2693 ) ) GLOBAL_UNIT_ASSIGNED_CONTEXT ( ( #14712, #21941, #12932 ) ) REPRESENTATION_CONTEXT ( 'NONE', 'WORKASPACE' ) );
#749=CARTESIAN_POINT ( 'NONE',  ( 39.27359436029429673, 22.26288585089429972, 13.00000000000000000 ) ) ;
#755=FACE_OUTER_BOUND ( 'NONE', #14144, .T. ) ;
#804=CYLINDRICAL_SURFACE ( 'NONE', #4227, 4.250000000000000000 ) ;
#840=ADVANCED_FACE ( 'NONE', ( #2911 ), #9485, .F. ) ;
#864=CIRCLE ( 'NONE', #13389, 2.500000000000000444 ) ;
#900=ORIENTED_EDGE ( 'NONE', *, *, #21861, .T. ) ;
#917=FACE_OUTER_BOUND ( 'NONE', #4736, .T. ) ;
#925=ADVANCED_FACE ( 'NONE', ( #755, #13953 ), #20960, .T. ) ;
#961=ORIENTED_EDGE ( 'NONE', *, *, #1763, .T. ) ;
#980=EDGE_CURVE ( 'NONE', #677, #22280, #5671, .T. ) ;
#1010=DIRECTION ( 'NONE',  ( 0.000000000000000000, 0.000000000000000000, 1.000000000000000000 ) ) ;
#1022=CARTESIAN_POINT ( 'NONE',  ( 34.94102482032229773, 25.66320561742219653, 13.00000000000000000 ) ) ;
#1298=ORIENTED_EDGE ( 'NONE', *, *, #657, .T. ) ;
#1344=CARTESIAN_POINT ( 'NONE',  ( 36.57467860885130051, 21.71590586959139912, 15.00000000000000000 ) ) ;
#1348=AXIS2_PLACEMENT_3D ( 'NONE', #633, #22359, #20603 ) ;
#1373=ORIENTED_EDGE ( 'NONE', *, *, #21584, .T. ) ;
#1378=AXIS2_PLACEMENT_3D ( 'NONE', #1986, #9243, #4005 ) ;
#1404=ORIENTED_EDGE ( 'NONE', *, *, #2072, .T. ) ;
#1426=EDGE_CURVE ( 'NONE', #22280, #677, #7876, .T. ) ;
#1509=EDGE_CURVE ( 'NONE', #21424, #16953, #17974, .T. ) ;
#1525=VECTOR ( 'NONE', #3468, 1000.000000000000000 ) ;
#1538=ADVANCED_FACE ( 'NONE', ( #21280 ), #17622, .F. ) ;
#1676=DIRECTION ( 'NONE',  ( 0.000000000000000000, 0.000000000000000000, 1.000000000000000000 ) ) ;
#1738=DIRECTION ( 'NONE',  ( -0.9730401042858036753, 0.2306359803922031493, 5.432877459303543355E-17 ) ) ;
#1763=EDGE_CURVE ( 'NONE', #16953, #23364, #21851, .T. ) ;
#1784=CARTESIAN_POINT ( 'NONE',  ( 34.40839383886530101, 23.41606575285529956, 9.720299461620768966 ) ) ;
#1843=ORIENTED_EDGE ( 'NONE', *, *, #16910, .T. ) ;
#1854=AXIS2_PLACEMENT_3D ( 'NONE', #12756, #14760, #17994 ) ;
#1986=CARTESIAN_POINT ( 'NONE',  ( 36.84099409957980242, 22.83947580187480142, 13.00000000000000000 ) ) ;
#2064=PLANE ( 'NONE',  #18503 ) ;
#2072=EDGE_CURVE ( 'NONE', #4537, #3647, #21376, .T. ) ;
#2113=EDGE_CURVE ( 'NONE', #8342, #16244, #14243, .T. ) ;
#2144=VECTOR ( 'NONE', #2623, 999.9999999999998863 ) ;
#2155=LINE ( 'NONE', #20565, #4947 ) ;
#2165=ADVANCED_FACE ( 'NONE', ( #16397 ), #5155, .T. ) ;
#2201=CARTESIAN_POINT ( 'NONE',  ( 36.30836311812279860, 20.59233593730800038, 13.00000000000000000 ) ) ;
#2217=CARTESIAN_POINT ( 'NONE',  ( 37.13840842239409312, 23.31972727237329934, 15.00000000000000000 ) ) ;
#2222=ORIENTED_EDGE ( 'NONE', *, *, #17682, .T. ) ;
#2455=( BOUNDED_CURVE ( )  B_SPLINE_CURVE ( 2, ( #20488, #291, #2201 ),
 .UNSPECIFIED., .F., .F. ) 
 B_SPLINE_CURVE_WITH_KNOTS ( ( 3, 3 ),
 ( 0.000000000000000000, 0.2336872276155859962 ),
 .UNSPECIFIED. ) 
 CURVE ( )  GEOMETRIC_REPRESENTATION_ITEM ( )  RATIONAL_B_SPLINE_CURVE ( ( 1.000000000000000000, 1.154700538379259900, 1.000000000000000000 ) ) 
 REPRESENTATION_ITEM ( '' )  );
#2495=ORIENTED_EDGE ( 'NONE', *, *, #7190, .F. ) ;
#2508=EDGE_CURVE ( 'NONE', #10083, #7364, #5527, .T. ) ;
#2511=DIRECTION ( 'NONE',  ( 0.000000000000000000, 0.000000000000000000, 1.000000000000000000 ) ) ;
#2522=CARTESIAN_POINT ( 'NONE',  ( 34.94102482032229773, 25.66320561742219653, 13.00000000000000000 ) ) ;
#2530=ORIENTED_EDGE ( 'NONE', *, *, #8422, .T. ) ;
#2569=CARTESIAN_POINT ( 'NONE',  ( 0.000000000000000000, 0.000000000000000000, 0.000000000000000000 ) ) ;
#2623=DIRECTION ( 'NONE',  ( 0.2306359803922028995, 0.9730401042858036753, -9.756037151021835575E-16 ) ) ;
#2693=UNCERTAINTY_MEASURE_WITH_UNIT (LENGTH_MEASURE( 1.000000000000000082E-05 ), #14712, 'distance_accuracy_value', 'NONE');
#2720=AXIS2_PLACEMENT_3D ( 'NONE', #6693, #7049, #1676 ) ;
#2742=EDGE_CURVE ( 'NONE', #20392, #23222, #11283, .T. ) ;
#2763=VECTOR ( 'NONE', #8499, 1000.000000000000114 ) ;
#2778=AXIS2_PLACEMENT_3D ( 'NONE', #6525, #13776, #5103 ) ;
#2854=EDGE_LOOP ( 'NONE', ( #17338, #4452, #20216, #2530, #10256 ) ) ;
#2874=DIRECTION ( 'NONE',  ( -0.9730401042858036753, 0.2306359803922028995, 5.959266323858677443E-17 ) ) ;
#2911=FACE_OUTER_BOUND ( 'NONE', #16737, .T. ) ;
#3010=DIRECTION ( 'NONE',  ( -0.6880432561069586006, 0.1630842657209347069, -0.7071067811865459074 ) ) ;
#3026=EDGE_CURVE ( 'NONE', #7364, #10083, #21102, .T. ) ;
#3051=PRODUCT_DEFINITION ( 'UNKNOWN', '', #4225, #23214 ) ;
#3057=DIRECTION ( 'NONE',  ( -0.9730401042858036753, 0.2306359803922028995, 5.959266323858677443E-17 ) ) ;
#3109=ORIENTED_EDGE ( 'NONE', *, *, #14116, .T. ) ;
#3116=CARTESIAN_POINT ( 'NONE',  ( 34.67470932959380292, 24.53963568513870186, 15.00000000000000000 ) ) ;
#3199=DIRECTION ( 'NONE',  ( -0.9730401042858036753, 0.2306359803922031493, 5.432877459303543355E-17 ) ) ;
#3221=CARTESIAN_POINT ( 'NONE',  ( 34.67470932959380292, 24.53963568513870186, 11.00000000000000000 ) ) ;
#3412=DIRECTION ( 'NONE',  ( 0.9730401042858035643, -0.2306359803922028717, -5.432877459303547053E-17 ) ) ;
#3428=ORIENTED_EDGE ( 'NONE', *, *, #4168, .T. ) ;
#3466=DIRECTION ( 'NONE',  ( 1.000000000000000000, 0.000000000000000000, 0.000000000000000000 ) ) ;
#3468=DIRECTION ( 'NONE',  ( -0.4865200521429013936, 0.1153179901961013387, -0.8660254037844388186 ) ) ;
#3544=CYLINDRICAL_SURFACE ( 'NONE', #1378, 4.250000000000000000 ) ;
#3549=AXIS2_PLACEMENT_3D ( 'NONE', #3878, #1738, #9003 ) ;
#3616=CARTESIAN_POINT ( 'NONE',  ( 38.67394081127457639, 19.73298157975121470, 13.00000000000000000 ) ) ;
#3646=DIRECTION ( 'NONE',  ( 0.000000000000000000, 0.000000000000000000, -1.000000000000000000 ) ) ;
#3647=VERTEX_POINT ( 'NONE', #17886 ) ;
#3661=EDGE_LOOP ( 'NONE', ( #11902, #21846, #23394, #7749, #10464 ) ) ;
#3679=( BOUNDED_CURVE ( )  B_SPLINE_CURVE ( 2, ( #14616, #9273, #14961 ),
 .UNSPECIFIED., .F., .F. ) 
 B_SPLINE_CURVE_WITH_KNOTS ( ( 3, 3 ),
 ( 0.000000000000000000, 0.1168436138077860315 ),
 .UNSPECIFIED. ) 
 CURVE ( )  GEOMETRIC_REPRESENTATION_ITEM ( )  RATIONAL_B_SPLINE_CURVE ( ( 1.000000000000000000, 1.077350269189620402, 1.077350269189624843 ) ) 
 REPRESENTATION_ITEM ( '' )  );
#3758=EDGE_LOOP ( 'NONE', ( #14593, #21185, #23005, #14005 ) ) ;
#3878=CARTESIAN_POINT ( 'NONE',  ( 34.89491389100820129, 23.30074776265919922, 13.00000000000000000 ) ) ;
#3886=FACE_OUTER_BOUND ( 'NONE', #14180, .T. ) ;
#3893=VECTOR ( 'NONE', #6366, 1000.000000000000114 ) ;
#3906=DIRECTION ( 'NONE',  ( 0.9730401042858035643, -0.2306359803922028717, -5.959266323858677443E-17 ) ) ;
#3910=SHAPE_REPRESENTATION_RELATIONSHIP ( 'NONE' , 'NONE' ,  #10862, #17868 ) ;
#3959=DIRECTION ( 'NONE',  ( 0.000000000000000000, 0.000000000000000000, 1.000000000000000000 ) ) ;
#3966=CARTESIAN_POINT ( 'NONE',  ( 34.67470932959380292, 24.53963568513870186, 11.00000000000000000 ) ) ;
#3981=ORIENTED_EDGE ( 'NONE', *, *, #4300, .F. ) ;
#4000=CARTESIAN_POINT ( 'NONE',  ( 49.97703550743810297, 19.72589006658010291, 13.00000000000000000 ) ) ;
#4005=DIRECTION ( 'NONE',  ( 0.000000000000000000, 0.000000000000000000, -1.000000000000000000 ) ) ;
#4020=CARTESIAN_POINT ( 'NONE',  ( 37.37362508103680625, 25.08661566644159890, 13.00000000000000000 ) ) ;
#4098=VECTOR ( 'NONE', #20359, 999.9999999999998863 ) ;
#4119=VERTEX_POINT ( 'NONE', #20365 ) ;
#4164=CARTESIAN_POINT ( 'NONE',  ( 35.89100945995100034, 24.25134070964849897, 15.00000000000000000 ) ) ;
#4167=CARTESIAN_POINT ( 'NONE',  ( 36.89121352362748496, 22.27682603178741516, 11.00000000000000000 ) ) ;
#4168=EDGE_CURVE ( 'NONE', #17440, #4537, #17636, .T. ) ;
#4222=ORIENTED_EDGE ( 'NONE', *, *, #15354, .F. ) ;
#4225=PRODUCT_DEFINITION_FORMATION_WITH_SPECIFIED_SOURCE ( 'ANY', '', #12718, .NOT_KNOWN. ) ;
#4227=AXIS2_PLACEMENT_3D ( 'NONE', #15312, #4852, #4622 ) ;
#4242=ORIENTED_EDGE ( 'NONE', *, *, #12170, .T. ) ;
#4273=AXIS2_PLACEMENT_3D ( 'NONE', #6781, #14006, #8911 ) ;
#4300=EDGE_CURVE ( 'NONE', #20392, #12727, #12407, .T. ) ;
#4388=CARTESIAN_POINT ( 'NONE',  ( 37.48968750243700043, 22.68571848161329996, 13.00000000000000000 ) ) ;
#4452=ORIENTED_EDGE ( 'NONE', *, *, #13697, .T. ) ;
#4537=VERTEX_POINT ( 'NONE', #2522 ) ;
#4555=DIRECTION ( 'NONE',  ( -0.9730401042858035643, 0.2306359803922028717, 5.959266323858677443E-17 ) ) ;
#4570=DIRECTION ( 'NONE',  ( -0.9730401042858035643, 0.2306359803922028717, 5.432877459303547053E-17 ) ) ;
#4589=CARTESIAN_POINT ( 'NONE',  ( 35.75979881747896627, 26.94964815373096556, 13.00000000000000000 ) ) ;
#4605=ORIENTED_EDGE ( 'NONE', *, *, #16927, .T. ) ;
#4622=DIRECTION ( 'NONE',  ( 0.000000000000000000, 0.000000000000000000, -1.000000000000000000 ) ) ;
#4669=ORIENTED_EDGE ( 'NONE', *, *, #21173, .T. ) ;
#4678=CIRCLE ( 'NONE', #5811, 2.500000000000000444 ) ;
#4736=EDGE_LOOP ( 'NONE', ( #13626, #20753, #18295, #4669, #13833 ) ) ;
#4765=CARTESIAN_POINT ( 'NONE',  ( 58.49563186522070168, 17.70675969991889787, 13.00000000000000000 ) ) ;
#4767=ORIENTED_EDGE ( 'NONE', *, *, #1509, .T. ) ;
#4777=EDGE_CURVE ( 'NONE', #12098, #11662, #7152, .T. ) ;
#4823=CARTESIAN_POINT ( 'NONE',  ( 34.27523609350100031, 22.85428078671360197, 15.00000000000000000 ) ) ;
#4845=AXIS2_PLACEMENT_3D ( 'NONE', #12090, #6731, #13852 ) ;
#4852=DIRECTION ( 'NONE',  ( 0.9730401042858035643, -0.2306359803922028717, -5.432877459303547053E-17 ) ) ;
#4902=DIRECTION ( 'NONE',  ( 0.9286452767786566032, 1.871119812896368998E-17, -0.3709689338970208472 ) ) ;
#4947=VECTOR ( 'NONE', #9415, 1000.000000000000114 ) ;
#4999=VERTEX_POINT ( 'NONE', #22198 ) ;
#5004=CARTESIAN_POINT ( 'NONE',  ( 37.01481097301077483, 22.79827665208033238, 15.00000000000000355 ) ) ;
#5022=AXIS2_PLACEMENT_3D ( 'NONE', #1784, #14385, #21615 ) ;
#5098=CYLINDRICAL_SURFACE ( 'NONE', #15227, 2.500000000000000444 ) ;
#5103=DIRECTION ( 'NONE',  ( 0.000000000000000000, 0.000000000000000000, 1.000000000000000000 ) ) ;
#5155=TOROIDAL_SURFACE ( 'NONE', #18443, 3.750000000000000000, 0.5000000000000000000 ) ;
#5177=CARTESIAN_POINT ( 'NONE',  ( 58.73439644601039333, 17.65016624305030035, 13.00000000000000000 ) ) ;
#5197=CARTESIAN_POINT ( 'NONE',  ( 34.89491389100820129, 23.30074776265920278, 8.749999999999998224 ) ) ;
#5200=VECTOR ( 'NONE', #19305, 1000.000000000000114 ) ;
#5264=CARTESIAN_POINT ( 'NONE',  ( 39.37089837072289811, 22.23982225285509884, 13.00000000000000000 ) ) ;
#5307=CYLINDRICAL_SURFACE ( 'NONE', #11173, 2.500000000000000444 ) ;
#5373=CONICAL_SURFACE ( 'NONE', #5743, 1.154700538379250796, 1.047197551196598297 ) ;
#5430=VECTOR ( 'NONE', #6923, 999.9999999999998863 ) ;
#5434=ORIENTED_EDGE ( 'NONE', *, *, #17059, .F. ) ;
#5476=CARTESIAN_POINT ( 'NONE',  ( 49.97703550743810297, 19.72589006658010291, 15.50000000000000000 ) ) ;
#5492=EDGE_CURVE ( 'NONE', #16244, #4999, #16633, .T. ) ;
#5527=CIRCLE ( 'NONE', #1348, 3.750000000000001776 ) ;
#5541=FACE_OUTER_BOUND ( 'NONE', #7399, .T. ) ;
#5671=CIRCLE ( 'NONE', #19345, 2.600000000000000089 ) ;
#5709=VERTEX_POINT ( 'NONE', #1344 ) ;
#5743=AXIS2_PLACEMENT_3D ( 'NONE', #4388, #11656, #18885 ) ;
#5809=CARTESIAN_POINT ( 'NONE',  ( 37.10730959030829723, 23.96304573415820016, 15.00000000000000000 ) ) ;
#5811=AXIS2_PLACEMENT_3D ( 'NONE', #23254, #18039, #6884 ) ;
#5898=ADVANCED_FACE ( 'NONE', ( #14648 ), #16643, .T. ) ;
#5962=AXIS2_PLACEMENT_3D ( 'NONE', #19151, #10024, #17252 ) ;
#6009=CARTESIAN_POINT ( 'NONE',  ( 35.87511680767506306, 27.43616820587386229, 13.00000000000000000 ) ) ;
#6121=CARTESIAN_POINT ( 'NONE',  ( 39.87324790931403840, 24.79279012203739541, 13.00000000000000000 ) ) ;
#6139=AXIS2_PLACEMENT_3D ( 'NONE', #16695, #16354, #9350 ) ;
#6170=DIRECTION ( 'NONE',  ( 0.9730401042858036753, -0.2306359803922031493, -5.959266323858673745E-17 ) ) ;
#6184=ORIENTED_EDGE ( 'NONE', *, *, #18676, .F. ) ;
#6218=ORIENTED_EDGE ( 'NONE', *, *, #3026, .F. ) ;
#6228=DIRECTION ( 'NONE',  ( -0.1997366180463770735, -0.8426774492125654881, -0.4999999999999997780 ) ) ;
#6267=EDGE_CURVE ( 'NONE', #16935, #8586, #18948, .T. ) ;
#6298=ORIENTED_EDGE ( 'NONE', *, *, #17317, .T. ) ;
#6299=VERTEX_POINT ( 'NONE', #10260 ) ;
#6341=DIRECTION ( 'NONE',  ( 0.9730401042858036753, -0.2306359803922028995, -5.432877459303547669E-17 ) ) ;
#6359=EDGE_LOOP ( 'NONE', ( #6941, #21906 ) ) ;
#6360=AXIS2_PLACEMENT_3D ( 'NONE', #17492, #6228, #20815 ) ;
#6366=DIRECTION ( 'NONE',  ( -0.6880432561069586006, 0.1630842657209346236, 0.7071067811865459074 ) ) ;
#6428=ADVANCED_FACE ( 'NONE', ( #7048, #7158 ), #12953, .T. ) ;
#6463=ORIENTED_EDGE ( 'NONE', *, *, #980, .T. ) ;
#6468=CARTESIAN_POINT ( 'NONE',  ( 37.10730959030829723, 23.96304573415820016, 11.00000000000000000 ) ) ;
#6512=CIRCLE ( 'NONE', #19789, 4.250000000000001776 ) ;
#6515=CIRCLE ( 'NONE', #2720, 2.500000000000000444 ) ;
#6525=CARTESIAN_POINT ( 'NONE',  ( 58.25686728443110241, 17.76335315678750248, 13.00000000000000000 ) ) ;
#6553=FACE_OUTER_BOUND ( 'NONE', #21581, .T. ) ;
#6603=DIRECTION ( 'NONE',  ( -0.1153179901961009640, -0.4865200521429018377, -0.8660254037844385966 ) ) ;
#6663=ORIENTED_EDGE ( 'NONE', *, *, #17682, .F. ) ;
#6689=ORIENTED_EDGE ( 'NONE', *, *, #1509, .F. ) ;
#6693=CARTESIAN_POINT ( 'NONE',  ( 39.37089837072289811, 22.23982225285509884, 13.00000000000000000 ) ) ;
#6697=CARTESIAN_POINT ( 'NONE',  ( 37.48968750243700043, 22.68571848161329996, 11.84529946162074943 ) ) ;
#6731=DIRECTION ( 'NONE',  ( 0.9730401042858036753, -0.2306359803922031493, -5.432877459303553216E-17 ) ) ;
#6736=DIRECTION ( 'NONE',  ( -0.2306359803922028995, -0.9730401042858036753, 1.343075398093749487E-16 ) ) ;
#6777=EDGE_LOOP ( 'NONE', ( #20427, #3428, #1404, #14691, #15263, #11336 ) ) ;
#6781=CARTESIAN_POINT ( 'NONE',  ( 34.14207834813680620, 22.29249582057189727, 15.00000000000000000 ) ) ;
#6801=ORIENTED_EDGE ( 'NONE', *, *, #5492, .F. ) ;
#6822=ADVANCED_FACE ( 'NONE', ( #23023 ), #22789, .F. ) ;
#6850=CARTESIAN_POINT ( 'NONE',  ( 34.14207834813680620, 22.29249582057189727, 15.00000000000000000 ) ) ;
#6884=DIRECTION ( 'NONE',  ( 0.000000000000000000, 0.000000000000000000, 1.000000000000000000 ) ) ;
#6889=VECTOR ( 'NONE', #6736, 999.9999999999998863 ) ;
#6923=DIRECTION ( 'NONE',  ( -0.9730401042858036753, 0.2306359803922028995, 5.959266323858677443E-17 ) ) ;
#6936=EDGE_CURVE ( 'NONE', #16935, #677, #16403, .T. ) ;
#6941=ORIENTED_EDGE ( 'NONE', *, *, #1426, .F. ) ;
#6952=AXIS2_PLACEMENT_3D ( 'NONE', #16482, #18161, #18281 ) ;
#7008=ORIENTED_EDGE ( 'NONE', *, *, #21094, .F. ) ;
#7048=FACE_BOUND ( 'NONE', #6777, .T. ) ;
#7049=DIRECTION ( 'NONE',  ( -0.9730401042858035643, 0.2306359803922028717, 6.126766849694256332E-17 ) ) ;
#7120=EDGE_CURVE ( 'NONE', #6299, #19075, #12174, .T. ) ;
#7152=LINE ( 'NONE', #5476, #9111 ) ;
#7158=FACE_OUTER_BOUND ( 'NONE', #19583, .T. ) ;
#7190=EDGE_CURVE ( 'NONE', #23222, #11662, #8733, .T. ) ;
#7327=CARTESIAN_POINT ( 'NONE',  ( 37.01481097301078194, 22.79827665208033594, 11.00000000000000178 ) ) ;
#7343=CIRCLE ( 'NONE', #110, 2.500000000000000444 ) ;
#7364=VERTEX_POINT ( 'NONE', #21537 ) ;
#7399=EDGE_LOOP ( 'NONE', ( #15664, #7491, #8183, #3109, #21180 ) ) ;
#7477=CIRCLE ( 'NONE', #16182, 2.009240000000000581 ) ;
#7491=ORIENTED_EDGE ( 'NONE', *, *, #108, .F. ) ;
#7498=ORIENTED_EDGE ( 'NONE', *, *, #18676, .T. ) ;
#7569=ORIENTED_EDGE ( 'NONE', *, *, #20297, .T. ) ;
#7653=LINE ( 'NONE', #18589, #16834 ) ;
#7749=ORIENTED_EDGE ( 'NONE', *, *, #15354, .T. ) ;
#7809=ORIENTED_EDGE ( 'NONE', *, *, #20297, .F. ) ;
#7876=CIRCLE ( 'NONE', #10932, 2.600000000000000089 ) ;
#7924=( BOUNDED_CURVE ( )  B_SPLINE_CURVE ( 2, ( #12675, #21667, #7327 ),
 .UNSPECIFIED., .F., .F. ) 
 B_SPLINE_CURVE_WITH_KNOTS ( ( 3, 3 ),
 ( 0.000000000000000000, 0.1168436138077977582 ),
 .UNSPECIFIED. ) 
 CURVE ( )  GEOMETRIC_REPRESENTATION_ITEM ( )  RATIONAL_B_SPLINE_CURVE ( ( 1.000000000000000000, 1.077350269189633059, 1.077350269189629950 ) ) 
 REPRESENTATION_ITEM ( '' )  );
#8032=TOROIDAL_SURFACE ( 'NONE', #21294, 3.750000000000000000, 0.5000000000000000000 ) ;
#8154=LINE ( 'NONE', #17293, #5200 ) ;
#8155=DIRECTION ( 'NONE',  ( 0.9730401042858035643, -0.2306359803922028717, -5.959266323858677443E-17 ) ) ;
#8175=DIRECTION ( 'NONE',  ( -0.2306359803922028440, -0.9730401042858034533, -4.307366329831518561E-32 ) ) ;
#8183=ORIENTED_EDGE ( 'NONE', *, *, #19222, .F. ) ;
#8227=CARTESIAN_POINT ( 'NONE',  ( 35.35837847849400362, 22.00420084508159846, 11.00000000000000000 ) ) ;
#8249=DIRECTION ( 'NONE',  ( 0.000000000000000000, 0.000000000000000000, 1.000000000000000000 ) ) ;
#8257=LINE ( 'NONE', #12313, #8834 ) ;
#8302=DIRECTION ( 'NONE',  ( 0.000000000000000000, 0.000000000000000000, 1.000000000000000000 ) ) ;
#8342=VERTEX_POINT ( 'NONE', #5197 ) ;
#8349=AXIS2_PLACEMENT_3D ( 'NONE', #18847, #4570, #8510 ) ;
#8402=ADVANCED_FACE ( 'NONE', ( #5541 ), #5307, .T. ) ;
#8422=EDGE_CURVE ( 'NONE', #8342, #22529, #16436, .T. ) ;
#8444=CARTESIAN_POINT ( 'NONE',  ( 34.74128820227589642, 24.82052816820960217, 14.50000000000000000 ) ) ;
#8499=DIRECTION ( 'NONE',  ( 0.1153179901961009640, 0.4865200521429018377, 0.8660254037844385966 ) ) ;
#8510=DIRECTION ( 'NONE',  ( 0.000000000000000000, 0.000000000000000000, -1.000000000000000000 ) ) ;
#8539=CARTESIAN_POINT ( 'NONE',  ( 38.79430841974239286, 19.80722199214058676, 13.00000000000000000 ) ) ;
#8548=AXIS2_PLACEMENT_3D ( 'NONE', #20867, #19451, #8175 ) ;
#8586=VERTEX_POINT ( 'NONE', #22157 ) ;
#8658=CARTESIAN_POINT ( 'NONE',  ( 49.97703550743810297, 19.72589006658010291, 13.00000000000000000 ) ) ;
#8694=ORIENTED_EDGE ( 'NONE', *, *, #21421, .F. ) ;
#8709=AXIS2_PLACEMENT_3D ( 'NONE', #15930, #17840, #12157 ) ;
#8733=LINE ( 'NONE', #15745, #3893 ) ;
#8747=EDGE_LOOP ( 'NONE', ( #12701, #20329, #11658, #20259 ) ) ;
#8804=EDGE_CURVE ( 'NONE', #4537, #19075, #10192, .T. ) ;
#8834=VECTOR ( 'NONE', #6603, 1000.000000000000114 ) ;
#8852=ORIENTED_EDGE ( 'NONE', *, *, #2508, .F. ) ;
#8900=CARTESIAN_POINT ( 'NONE',  ( 35.35837847849400362, 22.00420084508159846, 15.00000000000000000 ) ) ;
#8911=DIRECTION ( 'NONE',  ( 1.000000000000000000, -8.896220237034308570E-17, 0.000000000000000000 ) ) ;
#9003=DIRECTION ( 'NONE',  ( 0.000000000000000000, 0.000000000000000000, 1.000000000000000000 ) ) ;
#9032=AXIS2_PLACEMENT_3D ( 'NONE', #16684, #8155, #13257 ) ;
#9111=VECTOR ( 'NONE', #18304, 999.9999999999998863 ) ;
#9112=DIRECTION ( 'NONE',  ( 0.9730401042858035643, -0.2306359803922028717, -5.432877459303547053E-17 ) ) ;
#9117=ADVANCED_FACE ( 'NONE', ( #13238 ), #16908, .F. ) ;
#9141=EDGE_CURVE ( 'NONE', #90, #4999, #7653, .T. ) ;
#9243=DIRECTION ( 'NONE',  ( 0.9730401042858035643, -0.2306359803922028717, -5.432877459303547053E-17 ) ) ;
#9273=CARTESIAN_POINT ( 'NONE',  ( 36.89121352362745654, 22.27682603178741161, 15.00000000000000178 ) ) ;
#9300=EDGE_LOOP ( 'NONE', ( #459, #10409, #17061, #12499, #17426 ) ) ;
#9334=LINE ( 'NONE', #16558, #14888 ) ;
#9350=DIRECTION ( 'NONE',  ( 1.000000000000000000, 0.000000000000000000, 0.000000000000000000 ) ) ;
#9403=LINE ( 'NONE', #18794, #2144 ) ;
#9415=DIRECTION ( 'NONE',  ( -0.4865200521429014491, 0.1153179901961012555, 0.8660254037844388186 ) ) ;
#9471=CARTESIAN_POINT ( 'NONE',  ( 37.10730959030829723, 23.96304573415820016, 15.00000000000000000 ) ) ;
#9485=CONICAL_SURFACE ( 'NONE', #8349, 1.154700538379250796, 1.047197551196598297 ) ;
#9489=MANIFOLD_SOLID_BREP ( 'Imported1', #23154 ) ;
#9499=ORIENTED_EDGE ( 'NONE', *, *, #7190, .T. ) ;
#9566=CARTESIAN_POINT ( 'NONE',  ( 33.87576285740830428, 21.16892588828849853, 13.00000000000000000 ) ) ;
#9595=ORIENTED_EDGE ( 'NONE', *, *, #20430, .F. ) ;
#9638=AXIS2_PLACEMENT_3D ( 'NONE', #16248, #3199, #17692 ) ;
#9660=DIRECTION ( 'NONE',  ( -0.9730401042858036753, 0.2306359803922031493, 5.432877459303543355E-17 ) ) ;
#9667=ORIENTED_EDGE ( 'NONE', *, *, #21584, .F. ) ;
#9702=EDGE_CURVE ( 'NONE', #21424, #16270, #2155, .T. ) ;
#9751=EDGE_LOOP ( 'NONE', ( #22875, #4605, #16944, #6463, #11345 ) ) ;
#9844=ADVANCED_FACE ( 'NONE', ( #6553 ), #20502, .T. ) ;
#10024=DIRECTION ( 'NONE',  ( -0.9730401042858035643, 0.2306359803922028717, 5.667427308550587516E-17 ) ) ;
#10083=VERTEX_POINT ( 'NONE', #11386 ) ;
#10192=LINE ( 'NONE', #14203, #11190 ) ;
#10210=CARTESIAN_POINT ( 'NONE',  ( 58.73439644601037912, 17.65016624305025061, 15.00923999999996461 ) ) ;
#10223=VERTEX_POINT ( 'NONE', #6850 ) ;
#10250=CARTESIAN_POINT ( 'NONE',  ( 35.09206298776550170, 20.88063091279819972, 13.00000000000000000 ) ) ;
#10256=ORIENTED_EDGE ( 'NONE', *, *, #15630, .F. ) ;
#10260=CARTESIAN_POINT ( 'NONE',  ( 37.10730959030829723, 23.96304573415820016, 15.00000000000000000 ) ) ;
#10270=PLANE ( 'NONE',  #6360 ) ;
#10362=EDGE_CURVE ( 'NONE', #3647, #10223, #19431, .T. ) ;
#10388=CARTESIAN_POINT ( 'NONE',  ( 36.30836311812279860, 20.59233593730800038, 13.00000000000000000 ) ) ;
#10409=ORIENTED_EDGE ( 'NONE', *, *, #4777, .T. ) ;
#10432=ORIENTED_EDGE ( 'NONE', *, *, #8422, .F. ) ;
#10433=DIRECTION ( 'NONE',  ( 0.000000000000000000, 1.000000000000000000, 0.000000000000000000 ) ) ;
#10445=ORIENTED_EDGE ( 'NONE', *, *, #2742, .T. ) ;
#10464=ORIENTED_EDGE ( 'NONE', *, *, #13020, .T. ) ;
#10468=ORIENTED_EDGE ( 'NONE', *, *, #4300, .T. ) ;
#10862=SHAPE_REPRESENTATION ( '1602p_c_44', ( #12739 ), #743 ) ;
#10882=VECTOR ( 'NONE', #12370, 1000.000000000000114 ) ;
#10927=FACE_OUTER_BOUND ( 'NONE', #3661, .T. ) ;
#10932=AXIS2_PLACEMENT_3D ( 'NONE', #19169, #22586, #22699 ) ;
#10940=DIRECTION ( 'NONE',  ( -0.2306359803922028995, -0.9730401042858035643, 3.648592655857288816E-32 ) ) ;
#11173=AXIS2_PLACEMENT_3D ( 'NONE', #4000, #9112, #3646 ) ;
#11190=VECTOR ( 'NONE', #12092, 999.9999999999998863 ) ;
#11283=CIRCLE ( 'NONE', #13146, 2.009240000000000581 ) ;
#11336=ORIENTED_EDGE ( 'NONE', *, *, #22062, .T. ) ;
#11345=ORIENTED_EDGE ( 'NONE', *, *, #21173, .F. ) ;
#11386=CARTESIAN_POINT ( 'NONE',  ( 35.27327876533606599, 27.06496614392705879, 13.00000000000000000 ) ) ;
#11416=ORIENTED_EDGE ( 'NONE', *, *, #2113, .F. ) ;
#11421=CARTESIAN_POINT ( 'NONE',  ( 58.25686728443110951, 17.76335315678753801, 15.50000000000000000 ) ) ;
#11583=APPLICATION_CONTEXT ( 'configuration controlled 3d designs of mechanical parts and assemblies' ) ;
#11656=DIRECTION ( 'NONE',  ( -0.9730401042858035643, 0.2306359803922028717, 5.432877459303547053E-17 ) ) ;
#11658=ORIENTED_EDGE ( 'NONE', *, *, #22062, .F. ) ;
#11662=VERTEX_POINT ( 'NONE', #11421 ) ;
#11713=DIRECTION ( 'NONE',  ( -0.9730401042858036753, 0.2306359803922023999, -1.110223024625155524E-17 ) ) ;
#11725=DIRECTION ( 'NONE',  ( 0.000000000000000000, 0.000000000000000000, -1.000000000000000000 ) ) ;
#11768=CARTESIAN_POINT ( 'NONE',  ( 34.89491389100820129, 23.30074776265919922, 13.00000000000000000 ) ) ;
#11852=CARTESIAN_POINT ( 'NONE',  ( 39.37089837072289811, 22.23982225285510239, 15.50000000000000000 ) ) ;
#11902=ORIENTED_EDGE ( 'NONE', *, *, #13697, .F. ) ;
#11929=FACE_OUTER_BOUND ( 'NONE', #17687, .T. ) ;
#11950=ADVANCED_FACE ( 'NONE', ( #17177 ), #13574, .F. ) ;
#11956=CARTESIAN_POINT ( 'NONE',  ( 58.73439644601039333, 17.65016624305030035, 13.00000000000000000 ) ) ;
#12070=CARTESIAN_POINT ( 'NONE',  ( 58.49563186522070168, 17.70675969991889787, 10.74537999999999904 ) ) ;
#12090=CARTESIAN_POINT ( 'NONE',  ( 39.27359436029429673, 22.26288585089429972, 13.00000000000000000 ) ) ;
#12092=DIRECTION ( 'NONE',  ( 0.9730401042858036753, -0.2306359803922028995, -5.959266323858677443E-17 ) ) ;
#12098=VERTEX_POINT ( 'NONE', #11852 ) ;
#12157=DIRECTION ( 'NONE',  ( 0.000000000000000000, 0.000000000000000000, 1.000000000000000000 ) ) ;
#12158=CARTESIAN_POINT ( 'NONE',  ( 34.89491389100820129, 23.30074776265920278, 17.25000000000000000 ) ) ;
#12170=EDGE_CURVE ( 'NONE', #4999, #16244, #23110, .T. ) ;
#12174=( BOUNDED_CURVE ( )  B_SPLINE_CURVE ( 2, ( #5809, #20295, #4020 ),
 .UNSPECIFIED., .F., .F. ) 
 B_SPLINE_CURVE_WITH_KNOTS ( ( 3, 3 ),
 ( 0.000000000000000000, 0.2336872276155859962 ),
 .UNSPECIFIED. ) 
 CURVE ( )  GEOMETRIC_REPRESENTATION_ITEM ( )  RATIONAL_B_SPLINE_CURVE ( ( 1.000000000000000000, 1.154700538379259900, 1.000000000000000000 ) ) 
 REPRESENTATION_ITEM ( '' )  );
#12192=EDGE_LOOP ( 'NONE', ( #19885, #4222, #10432, #19034, #19298 ) ) ;
#12265=DIRECTION ( 'NONE',  ( 0.000000000000000000, 0.000000000000000000, 1.000000000000000000 ) ) ;
#12287=CARTESIAN_POINT ( 'NONE',  ( 36.76586756491560237, 21.07724224331889573, 13.99999999999999822 ) ) ;
#12313=CARTESIAN_POINT ( 'NONE',  ( 33.94234173009040489, 21.44981837135929936, 13.50000000000000000 ) ) ;
#12319=CARTESIAN_POINT ( 'NONE',  ( 39.27359436029429673, 22.26288585089429972, 13.00000000000000000 ) ) ;
#12334=DIRECTION ( 'NONE',  ( -0.9730401042858035643, 0.2306359803922028717, 5.959266323858677443E-17 ) ) ;
#12370=DIRECTION ( 'NONE',  ( -0.1153179901961009640, -0.4865200521429018377, 0.8660254037844385966 ) ) ;
#12407=LINE ( 'NONE', #12070, #23230 ) ;
#12453=CARTESIAN_POINT ( 'NONE',  ( 36.57467860885130051, 21.71590586959139912, 11.00000000000000000 ) ) ;
#12499=ORIENTED_EDGE ( 'NONE', *, *, #14116, .F. ) ;
#12525=DIRECTION ( 'NONE',  ( -0.9730401042858035643, 0.2306359803922028717, 6.126766849694256332E-17 ) ) ;
#12553=AXIS2_PLACEMENT_3D ( 'NONE', #3116, #23167, #4902 ) ;
#12675=CARTESIAN_POINT ( 'NONE',  ( 37.10730959030829723, 23.96304573415820016, 11.00000000000000000 ) ) ;
#12696=DIRECTION ( 'NONE',  ( -0.2306359803922028995, -0.9730401042858035643, 3.648592655857288816E-32 ) ) ;
#12700=CARTESIAN_POINT ( 'NONE',  ( 39.94748832170340336, 24.67242251356961091, 13.00000000000000000 ) ) ;
#12701=ORIENTED_EDGE ( 'NONE', *, *, #657, .F. ) ;
#12711=TOROIDAL_SURFACE ( 'NONE', #8548, 2.600000000000000089, 0.1000000000000000056 ) ;
#12718=PRODUCT ( '1602p_c_44', '1602p_c_44', '', ( #486 ) ) ;
#12727=VERTEX_POINT ( 'NONE', #23173 ) ;
#12739=AXIS2_PLACEMENT_3D ( 'NONE', #2569, #13380, #415 ) ;
#12756=CARTESIAN_POINT ( 'NONE',  ( 58.73439644601039333, 17.65016624305030035, 11.75000000000000000 ) ) ;
#12875=FACE_OUTER_BOUND ( 'NONE', #15321, .T. ) ;
#12932=( NAMED_UNIT ( * ) SI_UNIT ( $, .STERADIAN. ) SOLID_ANGLE_UNIT ( ) );
#12953=PLANE ( 'NONE',  #5022 ) ;
#13020=EDGE_CURVE ( 'NONE', #90, #21956, #19296, .T. ) ;
#13114=CARTESIAN_POINT ( 'NONE',  ( 58.25686728443110241, 17.76335315678750248, 13.00000000000000000 ) ) ;
#13118=CARTESIAN_POINT ( 'NONE',  ( 33.91471097434134663, 19.16532731944453616, 13.00000000000000000 ) ) ;
#13128=LINE ( 'NONE', #10250, #13422 ) ;
#13146=AXIS2_PLACEMENT_3D ( 'NONE', #11956, #4555, #8249 ) ;
#13238=FACE_OUTER_BOUND ( 'NONE', #17261, .T. ) ;
#13257=DIRECTION ( 'NONE',  ( -0.2306359803922028440, -0.9730401042858034533, -4.307366329831518561E-32 ) ) ;
#13295=ORIENTED_EDGE ( 'NONE', *, *, #21861, .F. ) ;
#13351=CIRCLE ( 'NONE', #6139, 0.5000000000000004441 ) ;
#13357=LINE ( 'NONE', #15248, #4098 ) ;
#13380=DIRECTION ( 'NONE',  ( 0.000000000000000000, 0.000000000000000000, 1.000000000000000000 ) ) ;
#13389=AXIS2_PLACEMENT_3D ( 'NONE', #5264, #12525, #3959 ) ;
#13422=VECTOR ( 'NONE', #2874, 999.9999999999998863 ) ;
#13424=DIRECTION ( 'NONE',  ( 0.000000000000000000, 0.000000000000000000, 1.000000000000000000 ) ) ;
#13521=APPLICATION_CONTEXT ( 'configuration controlled 3d designs of mechanical parts and assemblies' ) ;
#13526=DIRECTION ( 'NONE',  ( -0.9730401042858036753, 0.2306359803922031493, 5.432877459303543355E-17 ) ) ;
#13556=AXIS2_PLACEMENT_3D ( 'NONE', #4589, #22741, #10433 ) ;
#13574=TOROIDAL_SURFACE ( 'NONE', #9032, 2.600000000000000089, 0.1000000000000000056 ) ;
#13576=FACE_OUTER_BOUND ( 'NONE', #8747, .T. ) ;
#13600=CARTESIAN_POINT ( 'NONE',  ( 37.56481403710121469, 24.44795204016919854, 12.00000000000000000 ) ) ;
#13601=VERTEX_POINT ( 'NONE', #19199 ) ;
#13626=ORIENTED_EDGE ( 'NONE', *, *, #6936, .F. ) ;
#13642=FACE_OUTER_BOUND ( 'NONE', #12192, .T. ) ;
#13697=EDGE_CURVE ( 'NONE', #10083, #21956, #15448, .T. ) ;
#13719=CARTESIAN_POINT ( 'NONE',  ( 39.27359436029429673, 22.26288585089429972, 9.625000000000000000 ) ) ;
#13754=FACE_OUTER_BOUND ( 'NONE', #531, .T. ) ;
#13776=DIRECTION ( 'NONE',  ( 0.9730401042858035643, -0.2306359803922028717, -5.432877459303547053E-17 ) ) ;
#13833=ORIENTED_EDGE ( 'NONE', *, *, #1426, .T. ) ;
#13844=DIRECTION ( 'NONE',  ( -9.594916218540590128E-33, 2.583840697242805182E-16, -1.000000000000000000 ) ) ;
#13852=DIRECTION ( 'NONE',  ( 0.000000000000000000, 0.000000000000000000, -1.000000000000000000 ) ) ;
#13907=DIRECTION ( 'NONE',  ( -0.9730401042858035643, 0.2306359803922028717, 5.667427308550587516E-17 ) ) ;
#13922=ORIENTED_EDGE ( 'NONE', *, *, #5492, .T. ) ;
#13953=FACE_BOUND ( 'NONE', #6359, .T. ) ;
#13982=ORIENTED_EDGE ( 'NONE', *, *, #9141, .T. ) ;
#14005=ORIENTED_EDGE ( 'NONE', *, *, #8804, .T. ) ;
#14006=DIRECTION ( 'NONE',  ( 1.040345436475888435E-32, 1.169424102322700040E-16, 1.000000000000000000 ) ) ;
#14116=EDGE_CURVE ( 'NONE', #8586, #12727, #13357, .T. ) ;
#14144=EDGE_LOOP ( 'NONE', ( #13922, #4242 ) ) ;
#14180=EDGE_LOOP ( 'NONE', ( #22072, #13982, #6801, #11416, #5434 ) ) ;
#14187=CARTESIAN_POINT ( 'NONE',  ( 37.37362508103680625, 25.08661566644159890, 13.00000000000000000 ) ) ;
#14189=ORIENTED_EDGE ( 'NONE', *, *, #10362, .F. ) ;
#14203=CARTESIAN_POINT ( 'NONE',  ( 36.15732495067950225, 25.37491064193190127, 13.00000000000000000 ) ) ;
#14209=ORIENTED_EDGE ( 'NONE', *, *, #9702, .T. ) ;
#14230=DIRECTION ( 'NONE',  ( 0.9730401042858035643, -0.2306359803922028717, -5.959266323858677443E-17 ) ) ;
#14243=LINE ( 'NONE', #17706, #22590 ) ;
#14295=DIRECTION ( 'NONE',  ( 0.000000000000000000, 0.000000000000000000, 1.000000000000000000 ) ) ;
#14385=DIRECTION ( 'NONE',  ( -0.9730401042858035643, 0.2306359803922028717, 5.959266323858679908E-17 ) ) ;
#14404=PRODUCT_DEFINITION_SHAPE ( 'NONE', 'NONE',  #3051 ) ;
#14543=AXIS2_PLACEMENT_3D ( 'NONE', #23473, #23295, #3466 ) ;
#14569=AXIS2_PLACEMENT_3D ( 'NONE', #9566, #392, #11713 ) ;
#14593=ORIENTED_EDGE ( 'NONE', *, *, #7120, .F. ) ;
#14616=CARTESIAN_POINT ( 'NONE',  ( 36.57467860885130051, 21.71590586959139912, 15.00000000000000000 ) ) ;
#14648=FACE_OUTER_BOUND ( 'NONE', #20266, .T. ) ;
#14691=ORIENTED_EDGE ( 'NONE', *, *, #10362, .T. ) ;
#14712=( LENGTH_UNIT ( ) NAMED_UNIT ( * ) SI_UNIT ( .MILLI., .METRE. ) );
#14760=DIRECTION ( 'NONE',  ( 0.9730401042858035643, -0.2306359803922028717, -5.959266323858674978E-17 ) ) ;
#14784=ADVANCED_FACE ( 'NONE', ( #11929 ), #23029, .T. ) ;
#14888=VECTOR ( 'NONE', #18136, 999.9999999999998863 ) ;
#14961=CARTESIAN_POINT ( 'NONE',  ( 37.01481097301077483, 22.79827665208033238, 15.00000000000000178 ) ) ;
#14974=CARTESIAN_POINT ( 'NONE',  ( 37.01481097301078194, 22.79827665208033594, 11.00000000000000178 ) ) ;
#15092=VECTOR ( 'NONE', #3057, 999.9999999999998863 ) ;
#15227=AXIS2_PLACEMENT_3D ( 'NONE', #8658, #3412, #19810 ) ;
#15248=CARTESIAN_POINT ( 'NONE',  ( 49.97703550743810297, 19.72589006658010291, 10.49999999999999822 ) ) ;
#15263=ORIENTED_EDGE ( 'NONE', *, *, #18987, .T. ) ;
#15307=ADVANCED_FACE ( 'NONE', ( #13642 ), #804, .T. ) ;
#15312=CARTESIAN_POINT ( 'NONE',  ( 36.84099409957980242, 22.83947580187480142, 13.00000000000000000 ) ) ;
#15321=EDGE_LOOP ( 'NONE', ( #6184, #7569, #8694, #373, #21844 ) ) ;
#15354=EDGE_CURVE ( 'NONE', #22529, #90, #6512, .T. ) ;
#15417=ADVANCED_FACE ( 'NONE', ( #20653 ), #5373, .F. ) ;
#15439=ADVANCED_FACE ( 'NONE', ( #18034 ), #5098, .T. ) ;
#15448=CIRCLE ( 'NONE', #13556, 0.5000000000000004441 ) ;
#15453=CARTESIAN_POINT ( 'NONE',  ( 39.27359436029429673, 22.26288585089429972, 8.749999999999998224 ) ) ;
#15466=ADVANCED_FACE ( 'NONE', ( #10927 ), #8032, .T. ) ;
#15495=CARTESIAN_POINT ( 'NONE',  ( 58.73439644601037912, 17.65016624305025061, 10.99076000000003361 ) ) ;
#15524=EDGE_CURVE ( 'NONE', #5709, #10223, #17916, .T. ) ;
#15564=ORIENTED_EDGE ( 'NONE', *, *, #15524, .T. ) ;
#15630=EDGE_CURVE ( 'NONE', #7364, #22529, #13351, .T. ) ;
#15664=ORIENTED_EDGE ( 'NONE', *, *, #4777, .F. ) ;
#15737=ORIENTED_EDGE ( 'NONE', *, *, #4168, .F. ) ;
#15745=CARTESIAN_POINT ( 'NONE',  ( 58.49563186522070168, 17.70675969991889787, 15.25461999999999918 ) ) ;
#15768=LINE ( 'NONE', #4164, #15092 ) ;
#15842=CARTESIAN_POINT ( 'NONE',  ( 34.87444594764019712, 25.38231313435129977, 12.50000000000000000 ) ) ;
#15930=CARTESIAN_POINT ( 'NONE',  ( 39.37089837072289811, 22.23982225285509884, 13.00000000000000000 ) ) ;
#16088=DIRECTION ( 'NONE',  ( 0.9730401042858035643, -0.2306359803922028717, -5.959266323858667582E-17 ) ) ;
#16182=AXIS2_PLACEMENT_3D ( 'NONE', #5177, #12334, #1010 ) ;
#16244=VERTEX_POINT ( 'NONE', #15453 ) ;
#16248=CARTESIAN_POINT ( 'NONE',  ( 34.89491389100820129, 23.30074776265919922, 13.00000000000000000 ) ) ;
#16270=VERTEX_POINT ( 'NONE', #5004 ) ;
#16354=DIRECTION ( 'NONE',  ( 5.798605125234323991E-17, -1.374421231021384554E-17, 1.000000000000000000 ) ) ;
#16397=FACE_OUTER_BOUND ( 'NONE', #2854, .T. ) ;
#16403=CIRCLE ( 'NONE', #6952, 0.09999999999999939493 ) ;
#16405=CIRCLE ( 'NONE', #2778, 2.500000000000000444 ) ;
#16436=CIRCLE ( 'NONE', #3549, 4.250000000000001776 ) ;
#16482=CARTESIAN_POINT ( 'NONE',  ( 39.97055191974263266, 24.76972652399818742, 13.00000000000000000 ) ) ;
#16540=DIRECTION ( 'NONE',  ( -2.829953705592110306E-16, -9.355573283744330345E-16, -1.000000000000000000 ) ) ;
#16554=ORIENTED_EDGE ( 'NONE', *, *, #20430, .T. ) ;
#16558=CARTESIAN_POINT ( 'NONE',  ( 35.89100945995100034, 24.25134070964849897, 11.00000000000000000 ) ) ;
#16631=ORIENTED_EDGE ( 'NONE', *, *, #476, .F. ) ;
#16633=CIRCLE ( 'NONE', #17846, 4.250000000000000000 ) ;
#16643=PLANE ( 'NONE',  #1854 ) ;
#16684=CARTESIAN_POINT ( 'NONE',  ( 39.37089837072289811, 22.23982225285509884, 13.00000000000000000 ) ) ;
#16695=CARTESIAN_POINT ( 'NONE',  ( 34.03002896453743631, 19.65184737158743289, 13.00000000000000000 ) ) ;
#16737=EDGE_LOOP ( 'NONE', ( #6689, #14209, #1373, #19925, #16554, #7498 ) ) ;
#16834=VECTOR ( 'NONE', #6341, 999.9999999999998863 ) ;
#16908=PLANE ( 'NONE',  #14569 ) ;
#16910=EDGE_CURVE ( 'NONE', #12727, #11662, #16405, .T. ) ;
#16927=EDGE_CURVE ( 'NONE', #12098, #16935, #4678, .T. ) ;
#16935=VERTEX_POINT ( 'NONE', #12700 ) ;
#16944=ORIENTED_EDGE ( 'NONE', *, *, #6936, .T. ) ;
#16953=VERTEX_POINT ( 'NONE', #23120 ) ;
#17037=CARTESIAN_POINT ( 'NONE',  ( 37.37362508103680625, 25.08661566644159890, 13.00000000000000000 ) ) ;
#17059=EDGE_CURVE ( 'NONE', #21956, #8342, #20235, .T. ) ;
#17061=ORIENTED_EDGE ( 'NONE', *, *, #16910, .F. ) ;
#17177=FACE_OUTER_BOUND ( 'NONE', #9751, .T. ) ;
#17252=DIRECTION ( 'NONE',  ( 0.000000000000000000, 0.000000000000000000, 1.000000000000000000 ) ) ;
#17261=EDGE_LOOP ( 'NONE', ( #7008, #6298, #113, #22854 ) ) ;
#17293=CARTESIAN_POINT ( 'NONE',  ( 34.07549947545469848, 22.01160333750100051, 11.50000000000000000 ) ) ;
#17317=EDGE_CURVE ( 'NONE', #20134, #4119, #13128, .T. ) ;
#17338=ORIENTED_EDGE ( 'NONE', *, *, #3026, .T. ) ;
#17407=DIRECTION ( 'NONE',  ( 0.9730401042858035643, -0.2306359803922028717, -5.959266323858674978E-17 ) ) ;
#17426=ORIENTED_EDGE ( 'NONE', *, *, #6267, .F. ) ;
#17440=VERTEX_POINT ( 'NONE', #3221 ) ;
#17492=CARTESIAN_POINT ( 'NONE',  ( 34.14207834813680620, 22.29249582057189727, 11.00000000000000000 ) ) ;
#17494=( BOUNDED_CURVE ( )  B_SPLINE_CURVE ( 2, ( #10388, #12287, #22697 ),
 .UNSPECIFIED., .F., .F. ) 
 B_SPLINE_CURVE_WITH_KNOTS ( ( 3, 3 ),
 ( 0.000000000000000000, 0.2336872276155859962 ),
 .UNSPECIFIED. ) 
 CURVE ( )  GEOMETRIC_REPRESENTATION_ITEM ( )  RATIONAL_B_SPLINE_CURVE ( ( 1.000000000000000000, 1.154700538379249908, 1.000000000000000000 ) ) 
 REPRESENTATION_ITEM ( '' )  );
#17622=PLANE ( 'NONE',  #12553 ) ;
#17636=LINE ( 'NONE', #15842, #2763 ) ;
#17682=EDGE_CURVE ( 'NONE', #5709, #16270, #3679, .T. ) ;
#17687=EDGE_LOOP ( 'NONE', ( #3981, #10445, #9499, #22116 ) ) ;
#17692=DIRECTION ( 'NONE',  ( 0.000000000000000000, 0.000000000000000000, 1.000000000000000000 ) ) ;
#17706=CARTESIAN_POINT ( 'NONE',  ( 36.84099409957980242, 22.83947580187480142, 8.749999999999998224 ) ) ;
#17784=CARTESIAN_POINT ( 'NONE',  ( 36.30836311812279860, 20.59233593730800038, 13.00000000000000000 ) ) ;
#17796=CARTESIAN_POINT ( 'NONE',  ( 34.89491389100820129, 23.30074776265919922, 13.00000000000000000 ) ) ;
#17840=DIRECTION ( 'NONE',  ( -0.9730401042858035643, 0.2306359803922028717, 6.126766849694256332E-17 ) ) ;
#17846=AXIS2_PLACEMENT_3D ( 'NONE', #749, #534, #11725 ) ;
#17868=ADVANCED_BREP_SHAPE_REPRESENTATION ( '', ( #9489, #12739 ), #743 ) ;
#17886=CARTESIAN_POINT ( 'NONE',  ( 34.67470932959380292, 24.53963568513870186, 15.00000000000000000 ) ) ;
#17916=LINE ( 'NONE', #8900, #22811 ) ;
#17936=DIRECTION ( 'NONE',  ( 0.9730401042858036753, -0.2306359803922028995, -5.432877459303547669E-17 ) ) ;
#17974=LINE ( 'NONE', #6697, #1525 ) ;
#17994=DIRECTION ( 'NONE',  ( -9.594916218540590128E-33, 2.583840697242805182E-16, -1.000000000000000000 ) ) ;
#18034=FACE_OUTER_BOUND ( 'NONE', #9300, .T. ) ;
#18039=DIRECTION ( 'NONE',  ( -0.9730401042858035643, 0.2306359803922028717, 6.126766849694256332E-17 ) ) ;
#18136=DIRECTION ( 'NONE',  ( -0.9730401042858036753, 0.2306359803922028995, 5.959266323858677443E-17 ) ) ;
#18161=DIRECTION ( 'NONE',  ( -8.623081276789554834E-17, -1.054188326053478339E-16, -1.000000000000000000 ) ) ;
#18281=DIRECTION ( 'NONE',  ( 0.000000000000000000, 1.000000000000000000, 0.000000000000000000 ) ) ;
#18295=ORIENTED_EDGE ( 'NONE', *, *, #19222, .T. ) ;
#18304=DIRECTION ( 'NONE',  ( 0.9730401042858036753, -0.2306359803922028995, -5.432877459303547669E-17 ) ) ;
#18443=AXIS2_PLACEMENT_3D ( 'NONE', #203, #3906, #10940 ) ;
#18503=AXIS2_PLACEMENT_3D ( 'NONE', #3966, #16540, #265 ) ;
#18589=CARTESIAN_POINT ( 'NONE',  ( 36.84099409957980242, 22.83947580187480142, 17.25000000000000000 ) ) ;
#18676=EDGE_CURVE ( 'NONE', #13601, #16953, #7924, .T. ) ;
#18794=CARTESIAN_POINT ( 'NONE',  ( 34.54155158422950223, 23.97785071899700071, 11.00000000000000000 ) ) ;
#18847=CARTESIAN_POINT ( 'NONE',  ( 37.48968750243700043, 22.68571848161329996, 13.00000000000000000 ) ) ;
#18852=AXIS2_PLACEMENT_3D ( 'NONE', #247, #6170, #13424 ) ;
#18885=DIRECTION ( 'NONE',  ( 0.000000000000000000, 0.000000000000000000, -1.000000000000000000 ) ) ;
#18948=CIRCLE ( 'NONE', #8709, 2.500000000000000444 ) ;
#18987=EDGE_CURVE ( 'NONE', #10223, #4119, #8257, .T. ) ;
#19034=ORIENTED_EDGE ( 'NONE', *, *, #2113, .T. ) ;
#19075=VERTEX_POINT ( 'NONE', #14187 ) ;
#19090=ORIENTED_EDGE ( 'NONE', *, *, #2742, .F. ) ;
#19151=CARTESIAN_POINT ( 'NONE',  ( 58.49563186522070168, 17.70675969991889787, 13.00000000000000000 ) ) ;
#19169=CARTESIAN_POINT ( 'NONE',  ( 39.27359436029429673, 22.26288585089429972, 13.00000000000000000 ) ) ;
#19199=CARTESIAN_POINT ( 'NONE',  ( 37.10730959030829723, 23.96304573415820016, 11.00000000000000000 ) ) ;
#19222=EDGE_CURVE ( 'NONE', #8586, #467, #864, .T. ) ;
#19296=CIRCLE ( 'NONE', #20048, 4.250000000000001776 ) ;
#19298=ORIENTED_EDGE ( 'NONE', *, *, #12170, .F. ) ;
#19305=DIRECTION ( 'NONE',  ( 0.1153179901961009640, 0.4865200521429018377, -0.8660254037844385966 ) ) ;
#19345=AXIS2_PLACEMENT_3D ( 'NONE', #12319, #16088, #14295 ) ;
#19431=LINE ( 'NONE', #4823, #6889 ) ;
#19451=DIRECTION ( 'NONE',  ( 0.9730401042858035643, -0.2306359803922028717, -5.959266323858677443E-17 ) ) ;
#19520=EDGE_CURVE ( 'NONE', #23364, #23217, #22815, .T. ) ;
#19583=EDGE_LOOP ( 'NONE', ( #6218, #8852 ) ) ;
#19789=AXIS2_PLACEMENT_3D ( 'NONE', #11768, #13526, #8302 ) ;
#19810=DIRECTION ( 'NONE',  ( 0.000000000000000000, 0.000000000000000000, -1.000000000000000000 ) ) ;
#19885=ORIENTED_EDGE ( 'NONE', *, *, #9141, .F. ) ;
#19925=ORIENTED_EDGE ( 'NONE', *, *, #7120, .T. ) ;
#19928=CARTESIAN_POINT ( 'NONE',  ( 37.01481097301077483, 22.79827665208033238, 15.00000000000000178 ) ) ;
#20043=EDGE_LOOP ( 'NONE', ( #22724, #4767, #961, #1298, #21237, #2222 ) ) ;
#20048=AXIS2_PLACEMENT_3D ( 'NONE', #20217, #9660, #2511 ) ;
#20134=VERTEX_POINT ( 'NONE', #17784 ) ;
#20216=ORIENTED_EDGE ( 'NONE', *, *, #17059, .T. ) ;
#20217=CARTESIAN_POINT ( 'NONE',  ( 34.89491389100820129, 23.30074776265919922, 13.00000000000000000 ) ) ;
#20235=CIRCLE ( 'NONE', #9638, 4.250000000000001776 ) ;
#20259=ORIENTED_EDGE ( 'NONE', *, *, #17317, .F. ) ;
#20266=EDGE_LOOP ( 'NONE', ( #13295, #19090 ) ) ;
#20295=CARTESIAN_POINT ( 'NONE',  ( 37.56481403710121469, 24.44795204016919854, 14.00000000000001066 ) ) ;
#20297=EDGE_CURVE ( 'NONE', #13601, #17440, #9334, .T. ) ;
#20329=ORIENTED_EDGE ( 'NONE', *, *, #19520, .T. ) ;
#20359=DIRECTION ( 'NONE',  ( 0.9730401042858036753, -0.2306359803922028995, -5.432877459303547669E-17 ) ) ;
#20365=CARTESIAN_POINT ( 'NONE',  ( 33.87576285740830428, 21.16892588828849853, 13.00000000000000000 ) ) ;
#20392=VERTEX_POINT ( 'NONE', #15495 ) ;
#20427=ORIENTED_EDGE ( 'NONE', *, *, #21421, .T. ) ;
#20430=EDGE_CURVE ( 'NONE', #19075, #13601, #20678, .T. ) ;
#20488=CARTESIAN_POINT ( 'NONE',  ( 36.57467860885130051, 21.71590586959139912, 11.00000000000000000 ) ) ;
#20502=CONICAL_SURFACE ( 'NONE', #22389, 2.254620000000000513, 0.7853981633974461696 ) ;
#20565=CARTESIAN_POINT ( 'NONE',  ( 37.48968750243700043, 22.68571848161329996, 14.15470053837925057 ) ) ;
#20603=DIRECTION ( 'NONE',  ( 0.000000000000000000, 0.000000000000000000, 1.000000000000000000 ) ) ;
#20653=FACE_OUTER_BOUND ( 'NONE', #20043, .T. ) ;
#20678=( BOUNDED_CURVE ( )  B_SPLINE_CURVE ( 2, ( #17037, #13600, #6468 ),
 .UNSPECIFIED., .F., .F. ) 
 B_SPLINE_CURVE_WITH_KNOTS ( ( 3, 3 ),
 ( 0.000000000000000000, 0.2336872276155859962 ),
 .UNSPECIFIED. ) 
 CURVE ( )  GEOMETRIC_REPRESENTATION_ITEM ( )  RATIONAL_B_SPLINE_CURVE ( ( 1.000000000000000000, 1.154700538379259900, 1.000000000000000000 ) ) 
 REPRESENTATION_ITEM ( '' )  );
#20753=ORIENTED_EDGE ( 'NONE', *, *, #6267, .T. ) ;
#20791=SHAPE_DEFINITION_REPRESENTATION ( #14404, #10862 ) ;
#20815=DIRECTION ( 'NONE',  ( 0.000000000000000000, 0.5102823824563427202, -0.8600069128528436968 ) ) ;
#20816=EDGE_CURVE ( 'NONE', #11662, #12727, #7343, .T. ) ;
#20867=CARTESIAN_POINT ( 'NONE',  ( 39.37089837072289811, 22.23982225285509884, 13.00000000000000000 ) ) ;
#20960=PLANE ( 'NONE',  #354 ) ;
#20997=PLANE ( 'NONE',  #556 ) ;
#21006=CARTESIAN_POINT ( 'NONE',  ( 34.14207834813680620, 22.29249582057189727, 11.00000000000000000 ) ) ;
#21094=EDGE_CURVE ( 'NONE', #20134, #5709, #17494, .T. ) ;
#21102=CIRCLE ( 'NONE', #18852, 3.750000000000001776 ) ;
#21173=EDGE_CURVE ( 'NONE', #467, #22280, #23242, .T. ) ;
#21180=ORIENTED_EDGE ( 'NONE', *, *, #20816, .F. ) ;
#21185=ORIENTED_EDGE ( 'NONE', *, *, #476, .T. ) ;
#21226=DIRECTION ( 'NONE',  ( -0.9730401042858036753, 0.2306359803922028995, 5.959266323858677443E-17 ) ) ;
#21237=ORIENTED_EDGE ( 'NONE', *, *, #21094, .T. ) ;
#21280=FACE_OUTER_BOUND ( 'NONE', #3758, .T. ) ;
#21294=AXIS2_PLACEMENT_3D ( 'NONE', #17796, #14230, #12696 ) ;
#21376=LINE ( 'NONE', #8444, #10882 ) ;
#21421=EDGE_CURVE ( 'NONE', #23217, #17440, #9403, .T. ) ;
#21424=VERTEX_POINT ( 'NONE', #346 ) ;
#21530=ADVANCED_FACE ( 'NONE', ( #3886 ), #3544, .T. ) ;
#21537=CARTESIAN_POINT ( 'NONE',  ( 33.54350891239453603, 19.76716536178353678, 13.00000000000000000 ) ) ;
#21581=EDGE_LOOP ( 'NONE', ( #900, #10468, #1843, #2495 ) ) ;
#21584=EDGE_CURVE ( 'NONE', #16270, #6299, #21716, .T. ) ;
#21615=DIRECTION ( 'NONE',  ( 6.124378941433959925E-17, 0.000000000000000000, 1.000000000000000000 ) ) ;
#21667=CARTESIAN_POINT ( 'NONE',  ( 37.13840842239409312, 23.31972727237329579, 11.00000000000000178 ) ) ;
#21716=( BOUNDED_CURVE ( )  B_SPLINE_CURVE ( 2, ( #19928, #2217, #9471 ),
 .UNSPECIFIED., .F., .F. ) 
 B_SPLINE_CURVE_WITH_KNOTS ( ( 3, 3 ),
 ( 0.1168436138077860315, 0.2336872276155859962 ),
 .UNSPECIFIED. ) 
 CURVE ( )  GEOMETRIC_REPRESENTATION_ITEM ( )  RATIONAL_B_SPLINE_CURVE ( ( 1.077350269189624843, 1.077350269189629506, 1.000000000000000000 ) ) 
 REPRESENTATION_ITEM ( '' )  );
#21844=ORIENTED_EDGE ( 'NONE', *, *, #1763, .F. ) ;
#21846=ORIENTED_EDGE ( 'NONE', *, *, #2508, .T. ) ;
#21851=( BOUNDED_CURVE ( )  B_SPLINE_CURVE ( 2, ( #14974, #4167, #21857 ),
 .UNSPECIFIED., .F., .F. ) 
 B_SPLINE_CURVE_WITH_KNOTS ( ( 3, 3 ),
 ( 0.1168436138077977582, 0.2336872276155859962 ),
 .UNSPECIFIED. ) 
 CURVE ( )  GEOMETRIC_REPRESENTATION_ITEM ( )  RATIONAL_B_SPLINE_CURVE ( ( 1.077350269189629950, 1.077350269189626841, 1.000000000000000000 ) ) 
 REPRESENTATION_ITEM ( '' )  );
#21857=CARTESIAN_POINT ( 'NONE',  ( 36.57467860885130051, 21.71590586959139912, 11.00000000000000000 ) ) ;
#21861=EDGE_CURVE ( 'NONE', #23222, #20392, #7477, .T. ) ;
#21906=ORIENTED_EDGE ( 'NONE', *, *, #980, .F. ) ;
#21941=( NAMED_UNIT ( * ) PLANE_ANGLE_UNIT ( ) SI_UNIT ( $, .RADIAN. ) );
#21956=VERTEX_POINT ( 'NONE', #6009 ) ;
#22062=EDGE_CURVE ( 'NONE', #4119, #23217, #8154, .T. ) ;
#22072=ORIENTED_EDGE ( 'NONE', *, *, #13020, .F. ) ;
#22116=ORIENTED_EDGE ( 'NONE', *, *, #20816, .T. ) ;
#22157=CARTESIAN_POINT ( 'NONE',  ( 39.37089837072289811, 22.23982225285510239, 10.49999999999999822 ) ) ;
#22198=CARTESIAN_POINT ( 'NONE',  ( 39.27359436029429673, 22.26288585089429972, 17.25000000000000000 ) ) ;
#22230=DIRECTION ( 'NONE',  ( 0.9730401042858035643, -0.2306359803922028717, -5.432877459303547053E-17 ) ) ;
#22280=VERTEX_POINT ( 'NONE', #3616 ) ;
#22359=DIRECTION ( 'NONE',  ( 0.9730401042858036753, -0.2306359803922031493, -5.959266323858673745E-17 ) ) ;
#22389=AXIS2_PLACEMENT_3D ( 'NONE', #4765, #13907, #12265 ) ;
#22430=ADVANCED_FACE ( 'NONE', ( #12875 ), #2064, .F. ) ;
#22529=VERTEX_POINT ( 'NONE', #13118 ) ;
#22575=ADVANCED_FACE ( 'NONE', ( #13576 ), #10270, .F. ) ;
#22586=DIRECTION ( 'NONE',  ( 0.9730401042858035643, -0.2306359803922028717, -5.959266323858667582E-17 ) ) ;
#22590=VECTOR ( 'NONE', #17936, 999.9999999999998863 ) ;
#22638=DIRECTION ( 'NONE',  ( 0.1997366180463766849, 0.8426774492125652660, -0.5000000000000004441 ) ) ;
#22697=CARTESIAN_POINT ( 'NONE',  ( 36.57467860885130051, 21.71590586959139912, 15.00000000000000000 ) ) ;
#22699=DIRECTION ( 'NONE',  ( 0.000000000000000000, 0.000000000000000000, 1.000000000000000000 ) ) ;
#22724=ORIENTED_EDGE ( 'NONE', *, *, #9702, .F. ) ;
#22741=DIRECTION ( 'NONE',  ( -8.623081276789554834E-17, -1.054188326053478339E-16, -1.000000000000000000 ) ) ;
#22789=PLANE ( 'NONE',  #4273 ) ;
#22811=VECTOR ( 'NONE', #21226, 999.9999999999998863 ) ;
#22815=LINE ( 'NONE', #8227, #5430 ) ;
#22854=ORIENTED_EDGE ( 'NONE', *, *, #15524, .F. ) ;
#22875=ORIENTED_EDGE ( 'NONE', *, *, #108, .T. ) ;
#22995=DIRECTION ( 'NONE',  ( -0.9286452767786568252, -1.871119812896369614E-17, -0.3709689338970204586 ) ) ;
#23005=ORIENTED_EDGE ( 'NONE', *, *, #2072, .F. ) ;
#23023=FACE_OUTER_BOUND ( 'NONE', #22, .T. ) ;
#23029=CONICAL_SURFACE ( 'NONE', #5962, 2.254620000000000513, 0.7853981633974461696 ) ;
#23110=CIRCLE ( 'NONE', #4845, 4.250000000000000000 ) ;
#23120=CARTESIAN_POINT ( 'NONE',  ( 37.01481097301078194, 22.79827665208033594, 11.00000000000000178 ) ) ;
#23154=CLOSED_SHELL ( 'NONE', ( #840, #21530, #2165, #9844, #15439, #11950, #324, #8402, #925, #14784, #5898, #15466, #6428, #15307, #9117, #22575, #22430, #340, #6822, #1538, #15417 ) ) ;
#23167=DIRECTION ( 'NONE',  ( 0.1997366180463769070, 0.8426774492125652660, 0.5000000000000003331 ) ) ;
#23173=CARTESIAN_POINT ( 'NONE',  ( 58.25686728443110951, 17.76335315678753801, 10.49999999999999822 ) ) ;
#23214=DESIGN_CONTEXT ( 'detailed design', #11583, 'design' ) ;
#23217=VERTEX_POINT ( 'NONE', #21006 ) ;
#23222=VERTEX_POINT ( 'NONE', #10210 ) ;
#23230=VECTOR ( 'NONE', #3010, 1000.000000000000114 ) ;
#23242=CIRCLE ( 'NONE', #14543, 0.1000000000000028644 ) ;
#23254=CARTESIAN_POINT ( 'NONE',  ( 39.37089837072289811, 22.23982225285509884, 13.00000000000000000 ) ) ;
#23275=ORIENTED_EDGE ( 'NONE', *, *, #8804, .F. ) ;
#23295=DIRECTION ( 'NONE',  ( 5.798605125234323991E-17, -1.374421231021384554E-17, 1.000000000000000000 ) ) ;
#23364=VERTEX_POINT ( 'NONE', #12453 ) ;
#23394=ORIENTED_EDGE ( 'NONE', *, *, #15630, .T. ) ;
#23473=CARTESIAN_POINT ( 'NONE',  ( 38.77124482170317066, 19.70991798171200671, 13.00000000000000000 ) ) ;
#23515=COLOUR_RGB('Deep Blue', 0.09019608, 0.27058824, 0.51372549);
#23516=FILL_AREA_STYLE_COLOUR('',#23515);
#23517=FILL_AREA_STYLE('',(#23516));
#23518=SURFACE_STYLE_FILL_AREA(#23517);
#23519=SURFACE_SIDE_STYLE('',(#23518));
#23520=SURFACE_STYLE_USAGE(.BOTH.,#23519);
#23521=PRESENTATION_STYLE_ASSIGNMENT((#23520));
#23615=STYLED_ITEM('',(#23521),#9489);
#23616=MECHANICAL_DESIGN_GEOMETRIC_PRESENTATION_REPRESENTATION('',(#23615),#743);
ENDSEC;
END-ISO-10303-21;
